ISO-10303-21;
HEADER;
/* Generated by software containing ST-Developer
 * from STEP Tools, Inc. (www.steptools.com) 
 */

FILE_DESCRIPTION(
/* description */ ('Guided pneumatic stop gate'),
/* implementation_level */ '2;1');

FILE_NAME(
/* name */ 'Socket Set Screw - M4x6.step',
/* time_stamp */ '2026-10-27T21:43:45-07:00',
/* author */ (''),
/* organization */ (''),
/* preprocessor_version */ 'ST-DEVELOPER v20.2',
/* originating_system */ 'Autodesk Translation Framework v15.17.0.0',
/* authorisation */ '');

FILE_SCHEMA (('AUTOMOTIVE_DESIGN { 1 0 10303 214 3 1 1 }'));
ENDSEC;

DATA;
#10=MECHANICAL_DESIGN_GEOMETRIC_PRESENTATION_REPRESENTATION('',(#568),#14392);
#445=CONICAL_SURFACE('',#9253,0.185,0.785398163397449);
#446=CONICAL_SURFACE('',#9257,0.1625,0.785398163397449);
#484=SHAPE_REPRESENTATION_RELATIONSHIP('SRR','None',#14621,#526);
#526=ADVANCED_BREP_SHAPE_REPRESENTATION('',(#606),#14383);
#568=STYLED_ITEM('',(#14898),#606);
#606=MANIFOLD_SOLID_BREP('Body1',#7912);
#806=FACE_BOUND('',#2199,.T.);
#1074=PLANE('',#9244);
#1075=PLANE('',#9245);
#1076=PLANE('',#9246);
#1077=PLANE('',#9247);
#1078=PLANE('',#9248);
#1079=PLANE('',#9249);
#1080=PLANE('',#9250);
#1081=PLANE('',#9251);
#1082=PLANE('',#9259);
#1525=FACE_OUTER_BOUND('',#2191,.T.);
#1526=FACE_OUTER_BOUND('',#2192,.T.);
#1527=FACE_OUTER_BOUND('',#2193,.T.);
#1528=FACE_OUTER_BOUND('',#2194,.T.);
#1529=FACE_OUTER_BOUND('',#2195,.T.);
#1530=FACE_OUTER_BOUND('',#2196,.T.);
#1531=FACE_OUTER_BOUND('',#2197,.T.);
#1532=FACE_OUTER_BOUND('',#2198,.T.);
#1533=FACE_OUTER_BOUND('',#2200,.T.);
#1534=FACE_OUTER_BOUND('',#2201,.T.);
#1535=FACE_OUTER_BOUND('',#2202,.T.);
#1536=FACE_OUTER_BOUND('',#2203,.T.);
#2191=EDGE_LOOP('',(#6966,#6967,#6968,#6969));
#2192=EDGE_LOOP('',(#6970,#6971,#6972,#6973));
#2193=EDGE_LOOP('',(#6974,#6975,#6976,#6977));
#2194=EDGE_LOOP('',(#6978,#6979,#6980,#6981));
#2195=EDGE_LOOP('',(#6982,#6983,#6984,#6985));
#2196=EDGE_LOOP('',(#6986,#6987,#6988,#6989));
#2197=EDGE_LOOP('',(#6990,#6991,#6992,#6993,#6994,#6995));
#2198=EDGE_LOOP('',(#6996));
#2199=EDGE_LOOP('',(#6997,#6998,#6999,#7000,#7001,#7002));
#2200=EDGE_LOOP('',(#7003,#7004,#7005,#7006));
#2201=EDGE_LOOP('',(#7007,#7008,#7009,#7010));
#2202=EDGE_LOOP('',(#7011,#7012,#7013,#7014));
#2203=EDGE_LOOP('',(#7015));
#2747=LINE('',#13839,#3292);
#2748=LINE('',#13841,#3293);
#2749=LINE('',#13843,#3294);
#2750=LINE('',#13844,#3295);
#2751=LINE('',#13847,#3296);
#2752=LINE('',#13849,#3297);
#2753=LINE('',#13850,#3298);
#2754=LINE('',#13853,#3299);
#2755=LINE('',#13855,#3300);
#2756=LINE('',#13856,#3301);
#2757=LINE('',#13859,#3302);
#2758=LINE('',#13861,#3303);
#2759=LINE('',#13862,#3304);
#2760=LINE('',#13865,#3305);
#2761=LINE('',#13867,#3306);
#2762=LINE('',#13868,#3307);
#2763=LINE('',#13870,#3308);
#2764=LINE('',#13871,#3309);
#2765=LINE('',#13879,#3310);
#2766=LINE('',#13883,#3311);
#2767=LINE('',#13887,#3312);
#3292=VECTOR('',#11572,1.);
#3293=VECTOR('',#11573,1.);
#3294=VECTOR('',#11574,1.);
#3295=VECTOR('',#11575,1.);
#3296=VECTOR('',#11578,1.);
#3297=VECTOR('',#11579,1.);
#3298=VECTOR('',#11580,1.);
#3299=VECTOR('',#11583,1.);
#3300=VECTOR('',#11584,1.);
#3301=VECTOR('',#11585,1.);
#3302=VECTOR('',#11588,1.);
#3303=VECTOR('',#11589,1.);
#3304=VECTOR('',#11590,1.);
#3305=VECTOR('',#11593,1.);
#3306=VECTOR('',#11594,1.);
#3307=VECTOR('',#11595,1.);
#3308=VECTOR('',#11598,1.);
#3309=VECTOR('',#11599,1.);
#3310=VECTOR('',#11610,0.185);
#3311=VECTOR('',#11615,0.2);
#3312=VECTOR('',#11620,0.1625);
#3696=CIRCLE('',#9252,0.17);
#3697=CIRCLE('',#9254,0.1954);
#3698=CIRCLE('',#9256,0.1954);
#3699=CIRCLE('',#9258,0.125);
#4268=VERTEX_POINT('',#13837);
#4269=VERTEX_POINT('',#13838);
#4270=VERTEX_POINT('',#13840);
#4271=VERTEX_POINT('',#13842);
#4272=VERTEX_POINT('',#13846);
#4273=VERTEX_POINT('',#13848);
#4274=VERTEX_POINT('',#13852);
#4275=VERTEX_POINT('',#13854);
#4276=VERTEX_POINT('',#13858);
#4277=VERTEX_POINT('',#13860);
#4278=VERTEX_POINT('',#13864);
#4279=VERTEX_POINT('',#13866);
#4280=VERTEX_POINT('',#13874);
#4281=VERTEX_POINT('',#13877);
#4282=VERTEX_POINT('',#13881);
#4283=VERTEX_POINT('',#13885);
#5181=EDGE_CURVE('',#4268,#4269,#2747,.T.);
#5182=EDGE_CURVE('',#4268,#4270,#2748,.T.);
#5183=EDGE_CURVE('',#4270,#4271,#2749,.T.);
#5184=EDGE_CURVE('',#4269,#4271,#2750,.T.);
#5185=EDGE_CURVE('',#4272,#4268,#2751,.T.);
#5186=EDGE_CURVE('',#4272,#4273,#2752,.T.);
#5187=EDGE_CURVE('',#4273,#4270,#2753,.T.);
#5188=EDGE_CURVE('',#4274,#4272,#2754,.T.);
#5189=EDGE_CURVE('',#4274,#4275,#2755,.T.);
#5190=EDGE_CURVE('',#4275,#4273,#2756,.T.);
#5191=EDGE_CURVE('',#4276,#4274,#2757,.T.);
#5192=EDGE_CURVE('',#4276,#4277,#2758,.T.);
#5193=EDGE_CURVE('',#4277,#4275,#2759,.T.);
#5194=EDGE_CURVE('',#4278,#4276,#2760,.T.);
#5195=EDGE_CURVE('',#4278,#4279,#2761,.T.);
#5196=EDGE_CURVE('',#4279,#4277,#2762,.T.);
#5197=EDGE_CURVE('',#4269,#4278,#2763,.T.);
#5198=EDGE_CURVE('',#4271,#4279,#2764,.T.);
#5199=EDGE_CURVE('',#4280,#4280,#3696,.T.);
#5200=EDGE_CURVE('',#4281,#4281,#3697,.T.);
#5201=EDGE_CURVE('',#4281,#4280,#2765,.T.);
#5202=EDGE_CURVE('',#4282,#4282,#3698,.F.);
#5203=EDGE_CURVE('',#4282,#4281,#2766,.T.);
#5204=EDGE_CURVE('',#4283,#4283,#3699,.T.);
#5205=EDGE_CURVE('',#4283,#4282,#2767,.T.);
#6966=ORIENTED_EDGE('',*,*,#5181,.F.);
#6967=ORIENTED_EDGE('',*,*,#5182,.T.);
#6968=ORIENTED_EDGE('',*,*,#5183,.T.);
#6969=ORIENTED_EDGE('',*,*,#5184,.F.);
#6970=ORIENTED_EDGE('',*,*,#5185,.F.);
#6971=ORIENTED_EDGE('',*,*,#5186,.T.);
#6972=ORIENTED_EDGE('',*,*,#5187,.T.);
#6973=ORIENTED_EDGE('',*,*,#5182,.F.);
#6974=ORIENTED_EDGE('',*,*,#5188,.F.);
#6975=ORIENTED_EDGE('',*,*,#5189,.T.);
#6976=ORIENTED_EDGE('',*,*,#5190,.T.);
#6977=ORIENTED_EDGE('',*,*,#5186,.F.);
#6978=ORIENTED_EDGE('',*,*,#5191,.F.);
#6979=ORIENTED_EDGE('',*,*,#5192,.T.);
#6980=ORIENTED_EDGE('',*,*,#5193,.T.);
#6981=ORIENTED_EDGE('',*,*,#5189,.F.);
#6982=ORIENTED_EDGE('',*,*,#5194,.F.);
#6983=ORIENTED_EDGE('',*,*,#5195,.T.);
#6984=ORIENTED_EDGE('',*,*,#5196,.T.);
#6985=ORIENTED_EDGE('',*,*,#5192,.F.);
#6986=ORIENTED_EDGE('',*,*,#5197,.F.);
#6987=ORIENTED_EDGE('',*,*,#5184,.T.);
#6988=ORIENTED_EDGE('',*,*,#5198,.T.);
#6989=ORIENTED_EDGE('',*,*,#5195,.F.);
#6990=ORIENTED_EDGE('',*,*,#5198,.F.);
#6991=ORIENTED_EDGE('',*,*,#5183,.F.);
#6992=ORIENTED_EDGE('',*,*,#5187,.F.);
#6993=ORIENTED_EDGE('',*,*,#5190,.F.);
#6994=ORIENTED_EDGE('',*,*,#5193,.F.);
#6995=ORIENTED_EDGE('',*,*,#5196,.F.);
#6996=ORIENTED_EDGE('',*,*,#5199,.F.);
#6997=ORIENTED_EDGE('',*,*,#5181,.T.);
#6998=ORIENTED_EDGE('',*,*,#5197,.T.);
#6999=ORIENTED_EDGE('',*,*,#5194,.T.);
#7000=ORIENTED_EDGE('',*,*,#5191,.T.);
#7001=ORIENTED_EDGE('',*,*,#5188,.T.);
#7002=ORIENTED_EDGE('',*,*,#5185,.T.);
#7003=ORIENTED_EDGE('',*,*,#5200,.F.);
#7004=ORIENTED_EDGE('',*,*,#5201,.T.);
#7005=ORIENTED_EDGE('',*,*,#5199,.T.);
#7006=ORIENTED_EDGE('',*,*,#5201,.F.);
#7007=ORIENTED_EDGE('',*,*,#5202,.F.);
#7008=ORIENTED_EDGE('',*,*,#5203,.T.);
#7009=ORIENTED_EDGE('',*,*,#5200,.T.);
#7010=ORIENTED_EDGE('',*,*,#5203,.F.);
#7011=ORIENTED_EDGE('',*,*,#5204,.F.);
#7012=ORIENTED_EDGE('',*,*,#5205,.T.);
#7013=ORIENTED_EDGE('',*,*,#5202,.T.);
#7014=ORIENTED_EDGE('',*,*,#5205,.F.);
#7015=ORIENTED_EDGE('',*,*,#5204,.T.);
#7383=CYLINDRICAL_SURFACE('',#9255,0.1954);
#7807=ADVANCED_FACE('',(#1525),#1074,.F.);
#7808=ADVANCED_FACE('',(#1526),#1075,.F.);
#7809=ADVANCED_FACE('',(#1527),#1076,.F.);
#7810=ADVANCED_FACE('',(#1528),#1077,.F.);
#7811=ADVANCED_FACE('',(#1529),#1078,.F.);
#7812=ADVANCED_FACE('',(#1530),#1079,.F.);
#7813=ADVANCED_FACE('',(#1531),#1080,.F.);
#7814=ADVANCED_FACE('',(#1532,#806),#1081,.T.);
#7815=ADVANCED_FACE('',(#1533),#445,.T.);
#7816=ADVANCED_FACE('',(#1534),#7383,.T.);
#7817=ADVANCED_FACE('',(#1535),#446,.T.);
#7818=ADVANCED_FACE('',(#1536),#1082,.T.);
#7912=CLOSED_SHELL('',(#7807,#7808,#7809,#7810,#7811,#7812,#7813,#7814,
#7815,#7816,#7817,#7818));
#9243=AXIS2_PLACEMENT_3D('',#13835,#11568,#11569);
#9244=AXIS2_PLACEMENT_3D('',#13836,#11570,#11571);
#9245=AXIS2_PLACEMENT_3D('',#13845,#11576,#11577);
#9246=AXIS2_PLACEMENT_3D('',#13851,#11581,#11582);
#9247=AXIS2_PLACEMENT_3D('',#13857,#11586,#11587);
#9248=AXIS2_PLACEMENT_3D('',#13863,#11591,#11592);
#9249=AXIS2_PLACEMENT_3D('',#13869,#11596,#11597);
#9250=AXIS2_PLACEMENT_3D('',#13872,#11600,#11601);
#9251=AXIS2_PLACEMENT_3D('',#13873,#11602,#11603);
#9252=AXIS2_PLACEMENT_3D('',#13875,#11604,#11605);
#9253=AXIS2_PLACEMENT_3D('',#13876,#11606,#11607);
#9254=AXIS2_PLACEMENT_3D('',#13878,#11608,#11609);
#9255=AXIS2_PLACEMENT_3D('',#13880,#11611,#11612);
#9256=AXIS2_PLACEMENT_3D('',#13882,#11613,#11614);
#9257=AXIS2_PLACEMENT_3D('',#13884,#11616,#11617);
#9258=AXIS2_PLACEMENT_3D('',#13886,#11618,#11619);
#9259=AXIS2_PLACEMENT_3D('',#13888,#11621,#11622);
#11568=DIRECTION('axis',(0.,0.,1.));
#11569=DIRECTION('refdir',(1.,0.,0.));
#11570=DIRECTION('center_axis',(0.866025403784439,0.,-0.5));
#11571=DIRECTION('ref_axis',(0.5,0.,0.866025403784439));
#11572=DIRECTION('',(0.5,0.,0.866025403784439));
#11573=DIRECTION('',(0.,-1.,0.));
#11574=DIRECTION('',(0.5,0.,0.866025403784439));
#11575=DIRECTION('',(0.,-1.,0.));
#11576=DIRECTION('center_axis',(1.20185167898973E-16,0.,-1.));
#11577=DIRECTION('ref_axis',(1.,0.,1.20185167898973E-16));
#11578=DIRECTION('',(1.,0.,1.20185167898973E-16));
#11579=DIRECTION('',(0.,-1.,0.));
#11580=DIRECTION('',(1.,0.,1.20185167898973E-16));
#11581=DIRECTION('center_axis',(-0.866025403784439,0.,-0.5));
#11582=DIRECTION('ref_axis',(0.5,0.,-0.866025403784439));
#11583=DIRECTION('',(0.5,0.,-0.866025403784439));
#11584=DIRECTION('',(0.,-1.,0.));
#11585=DIRECTION('',(0.5,0.,-0.866025403784439));
#11586=DIRECTION('center_axis',(-0.866025403784439,0.,0.5));
#11587=DIRECTION('ref_axis',(-0.5,0.,-0.866025403784439));
#11588=DIRECTION('',(-0.5,0.,-0.866025403784439));
#11589=DIRECTION('',(0.,-1.,0.));
#11590=DIRECTION('',(-0.5,0.,-0.866025403784439));
#11591=DIRECTION('center_axis',(-2.40370335797945E-16,0.,1.));
#11592=DIRECTION('ref_axis',(-1.,0.,-2.40370335797945E-16));
#11593=DIRECTION('',(-1.,0.,-2.40370335797945E-16));
#11594=DIRECTION('',(0.,-1.,0.));
#11595=DIRECTION('',(-1.,0.,-2.40370335797945E-16));
#11596=DIRECTION('center_axis',(0.866025403784439,0.,0.5));
#11597=DIRECTION('ref_axis',(-0.5,0.,0.866025403784439));
#11598=DIRECTION('',(-0.5,0.,0.866025403784439));
#11599=DIRECTION('',(-0.5,0.,0.866025403784439));
#11600=DIRECTION('center_axis',(0.,-1.,0.));
#11601=DIRECTION('ref_axis',(0.,0.,-1.));
#11602=DIRECTION('center_axis',(0.,1.,0.));
#11603=DIRECTION('ref_axis',(0.,0.,1.));
#11604=DIRECTION('center_axis',(0.,-1.,0.));
#11605=DIRECTION('ref_axis',(1.,0.,0.));
#11606=DIRECTION('center_axis',(0.,-1.,0.));
#11607=DIRECTION('ref_axis',(1.,0.,0.));
#11608=DIRECTION('center_axis',(0.,-1.,0.));
#11609=DIRECTION('ref_axis',(1.,0.,0.));
#11610=DIRECTION('',(0.707106781186548,0.707106781186547,8.65956056235494E-17));
#11611=DIRECTION('center_axis',(0.,-1.,0.));
#11612=DIRECTION('ref_axis',(1.,0.,0.));
#11613=DIRECTION('center_axis',(0.,1.,0.));
#11614=DIRECTION('ref_axis',(1.,0.,0.));
#11615=DIRECTION('',(0.,1.,0.));
#11616=DIRECTION('center_axis',(0.,1.,0.));
#11617=DIRECTION('ref_axis',(1.,0.,0.));
#11618=DIRECTION('center_axis',(0.,-1.,0.));
#11619=DIRECTION('ref_axis',(1.,0.,0.));
#11620=DIRECTION('',(-0.707106781186548,0.707106781186547,-8.65956056235494E-17));
#11621=DIRECTION('center_axis',(0.,-1.,0.));
#11622=DIRECTION('ref_axis',(0.,0.,-1.));
#13835=CARTESIAN_POINT('',(0.,0.,0.));
#13836=CARTESIAN_POINT('Origin',(0.0577350269189626,0.,-0.1));
#13837=CARTESIAN_POINT('',(0.0577350269189626,0.,-0.1));
#13838=CARTESIAN_POINT('',(0.115470053837925,0.,0.));
#13839=CARTESIAN_POINT('',(0.0934187836487032,0.,-0.0381939203391614));
#13840=CARTESIAN_POINT('',(0.0577350269189626,-0.2,-0.1));
#13841=CARTESIAN_POINT('',(0.0577350269189626,0.,-0.1));
#13842=CARTESIAN_POINT('',(0.115470053837925,-0.2,0.));
#13843=CARTESIAN_POINT('',(0.115470053837925,-0.2,0.));
#13844=CARTESIAN_POINT('',(0.115470053837925,0.,0.));
#13845=CARTESIAN_POINT('Origin',(-0.0577350269189626,0.,-0.1));
#13846=CARTESIAN_POINT('',(-0.0577350269189626,0.,-0.1));
#13847=CARTESIAN_POINT('',(0.0561324865405187,0.,-0.1));
#13848=CARTESIAN_POINT('',(-0.0577350269189626,-0.2,-0.1));
#13849=CARTESIAN_POINT('',(-0.0577350269189626,0.,-0.1));
#13850=CARTESIAN_POINT('',(0.0577350269189626,-0.2,-0.1));
#13851=CARTESIAN_POINT('Origin',(-0.115470053837925,0.,-1.38777878078145E-17));
#13852=CARTESIAN_POINT('',(-0.115470053837925,0.,-1.41410031829988E-17));
#13853=CARTESIAN_POINT('',(-0.0797862971081845,0.,-0.0618060796608387));
#13854=CARTESIAN_POINT('',(-0.115470053837925,-0.2,-1.38777878078145E-17));
#13855=CARTESIAN_POINT('',(-0.115470053837925,0.,-1.41410031829988E-17));
#13856=CARTESIAN_POINT('',(-0.0577350269189626,-0.2,-0.1));
#13857=CARTESIAN_POINT('Origin',(-0.0577350269189626,0.,0.1));
#13858=CARTESIAN_POINT('',(-0.0577350269189626,0.,0.1));
#13859=CARTESIAN_POINT('',(-0.0509187836487033,0.,0.111806079660839));
#13860=CARTESIAN_POINT('',(-0.0577350269189626,-0.2,0.1));
#13861=CARTESIAN_POINT('',(-0.0577350269189626,0.,0.1));
#13862=CARTESIAN_POINT('',(-0.115470053837925,-0.2,-1.41410031829988E-17));
#13863=CARTESIAN_POINT('Origin',(0.0577350269189626,0.,0.1));
#13864=CARTESIAN_POINT('',(0.0577350269189626,0.,0.1));
#13865=CARTESIAN_POINT('',(0.113867513459481,0.,0.1));
#13866=CARTESIAN_POINT('',(0.0577350269189626,-0.2,0.1));
#13867=CARTESIAN_POINT('',(0.0577350269189626,0.,0.1));
#13868=CARTESIAN_POINT('',(-0.0577350269189626,-0.2,0.1));
#13869=CARTESIAN_POINT('Origin',(0.115470053837925,0.,0.));
#13870=CARTESIAN_POINT('',(0.122286297108185,0.,-0.0118060796608386));
#13871=CARTESIAN_POINT('',(0.0577350269189626,-0.2,0.1));
#13872=CARTESIAN_POINT('Origin',(0.,-0.2,0.));
#13873=CARTESIAN_POINT('Origin',(0.17,0.,0.));
#13874=CARTESIAN_POINT('',(-0.17,-8.67361737988404E-18,-2.0818995585505E-17));
#13875=CARTESIAN_POINT('Origin',(0.,0.,0.));
#13876=CARTESIAN_POINT('Origin',(0.,-0.015,0.));
#13877=CARTESIAN_POINT('',(-0.1954,-0.0254,-2.39295984553393E-17));
#13878=CARTESIAN_POINT('Origin',(0.,-0.0254,0.));
#13879=CARTESIAN_POINT('',(-0.185,-0.015,-2.2655965784226E-17));
#13880=CARTESIAN_POINT('Origin',(0.,-0.2775,0.));
#13881=CARTESIAN_POINT('',(-0.1954,-0.5296,2.39295984553393E-17));
#13882=CARTESIAN_POINT('Origin',(0.,-0.5296,0.));
#13883=CARTESIAN_POINT('',(-0.1954,-0.2775,-2.39295984553393E-17));
#13884=CARTESIAN_POINT('Origin',(0.,-0.5625,0.));
#13885=CARTESIAN_POINT('',(-0.125,-0.6,-1.53080849893419E-17));
#13886=CARTESIAN_POINT('Origin',(0.,-0.6,0.));
#13887=CARTESIAN_POINT('',(-0.1625,-0.5625,-1.99005104861445E-17));
#13888=CARTESIAN_POINT('Origin',(0.,-0.6,0.));
#14335=UNCERTAINTY_MEASURE_WITH_UNIT(LENGTH_MEASURE(0.001),#14393,
'DISTANCE_ACCURACY_VALUE',
'Maximum model space distance between geometric entities at asserted c
onnectivities');
#14344=UNCERTAINTY_MEASURE_WITH_UNIT(LENGTH_MEASURE(0.001),#14393,
'DISTANCE_ACCURACY_VALUE',
'Maximum model space distance between geometric entities at asserted c
onnectivities');
#14383=(
GEOMETRIC_REPRESENTATION_CONTEXT(3)
GLOBAL_UNCERTAINTY_ASSIGNED_CONTEXT((#14335))
GLOBAL_UNIT_ASSIGNED_CONTEXT((#14393,#14395,#14396))
REPRESENTATION_CONTEXT('','3D')
);
#14392=(
GEOMETRIC_REPRESENTATION_CONTEXT(3)
GLOBAL_UNCERTAINTY_ASSIGNED_CONTEXT((#14344))
GLOBAL_UNIT_ASSIGNED_CONTEXT((#14393,#14395,#14396))
REPRESENTATION_CONTEXT('','3D')
);
#14393=(
LENGTH_UNIT()
NAMED_UNIT(*)
SI_UNIT(.CENTI.,.METRE.)
);
#14395=(
NAMED_UNIT(*)
PLANE_ANGLE_UNIT()
SI_UNIT($,.RADIAN.)
);
#14396=(
NAMED_UNIT(*)
SI_UNIT($,.STERADIAN.)
SOLID_ANGLE_UNIT()
);
#14435=SHAPE_DEFINITION_REPRESENTATION(#14554,#14621);
#14554=PRODUCT_DEFINITION_SHAPE('',$,#14669);
#14621=SHAPE_REPRESENTATION('',(#9243),#14383);
#14630=PRODUCT_DEFINITION_CONTEXT('part definition',#14773,'design');
#14669=PRODUCT_DEFINITION('Socket Set Screw - M4x6',
'Socket Set Screw - M4x6',#14716,#14630);
#14716=PRODUCT_DEFINITION_FORMATION('',$,#14813);
#14773=APPLICATION_CONTEXT(
'Core Data for Automotive Mechanical Design Process');
#14774=PRODUCT_CONTEXT('part definition',#14773,'mechanical');
#14813=PRODUCT('Socket Set Screw - M4x6','Socket Set Screw - M4x6',
'Socket Set Screw - M4x6',(#14774));
#14892=COLOUR_RGB('Black',0.12,0.14,0.17);
#14893=FILL_AREA_STYLE_COLOUR('',#14892);
#14894=FILL_AREA_STYLE('',(#14893));
#14895=SURFACE_STYLE_FILL_AREA(#14894);
#14896=SURFACE_SIDE_STYLE('',(#14895));
#14897=SURFACE_STYLE_USAGE(.BOTH.,#14896);
#14898=PRESENTATION_STYLE_ASSIGNMENT((#14897));
ENDSEC;
END-ISO-10303-21;
